ISO-10303-21;
HEADER;
/* Generated by software containing ST-Developer
 * from STEP Tools, Inc. (www.steptools.com) 
 */

FILE_DESCRIPTION(
/* description */ (''),
/* implementation_level */ '2;1');

FILE_NAME(
/* name */ 'Dovetail Base Rail.step',
/* time_stamp */ '2026-10-15T12:29:06-07:00',
/* author */ (''),
/* organization */ (''),
/* preprocessor_version */ 'ST-DEVELOPER v20.2',
/* originating_system */ 'Autodesk Translation Framework v15.15.0.0',
/* authorisation */ '');

FILE_SCHEMA (('AUTOMOTIVE_DESIGN { 1 0 10303 214 3 1 1 }'));
ENDSEC;

DATA;
#10=MECHANICAL_DESIGN_GEOMETRIC_PRESENTATION_REPRESENTATION('',(#1739),#135282);
#1713=SHAPE_REPRESENTATION_RELATIONSHIP('SRR','None',#135337,#1726);
#1726=ADVANCED_BREP_SHAPE_REPRESENTATION('',(#1752),#135269);
#1739=STYLED_ITEM('',(#135411),#1752);
#1752=MANIFOLD_SOLID_BREP('Body1',#32075);
#1765=CYLINDRICAL_SURFACE('',#32239,1.55);
#1766=CYLINDRICAL_SURFACE('',#32243,1.55);
#1767=CYLINDRICAL_SURFACE('',#32252,1.55);
#1768=CYLINDRICAL_SURFACE('',#32256,1.55);
#2016=FACE_BOUND('',#5102,.T.);
#2017=FACE_BOUND('',#5103,.T.);
#2018=FACE_BOUND('',#5111,.T.);
#2019=FACE_BOUND('',#5112,.T.);
#2232=PLANE('',#32237);
#2233=PLANE('',#32250);
#2234=PLANE('',#32260);
#2235=PLANE('',#32261);
#2236=PLANE('',#32262);
#2237=PLANE('',#32263);
#2238=PLANE('',#32264);
#2239=PLANE('',#32265);
#2240=PLANE('',#32266);
#2241=PLANE('',#32267);
#2242=PLANE('',#32268);
#2243=PLANE('',#32269);
#2244=PLANE('',#32270);
#2245=PLANE('',#32271);
#2246=PLANE('',#32272);
#2247=PLANE('',#32273);
#2248=PLANE('',#32274);
#2249=PLANE('',#32275);
#3346=FACE_OUTER_BOUND('',#5100,.T.);
#3347=FACE_OUTER_BOUND('',#5101,.T.);
#3348=FACE_OUTER_BOUND('',#5104,.T.);
#3349=FACE_OUTER_BOUND('',#5105,.T.);
#3350=FACE_OUTER_BOUND('',#5106,.T.);
#3351=FACE_OUTER_BOUND('',#5107,.T.);
#3352=FACE_OUTER_BOUND('',#5108,.T.);
#3353=FACE_OUTER_BOUND('',#5109,.T.);
#3354=FACE_OUTER_BOUND('',#5110,.T.);
#3355=FACE_OUTER_BOUND('',#5113,.T.);
#3356=FACE_OUTER_BOUND('',#5114,.T.);
#3357=FACE_OUTER_BOUND('',#5115,.T.);
#3358=FACE_OUTER_BOUND('',#5116,.T.);
#3359=FACE_OUTER_BOUND('',#5117,.T.);
#3360=FACE_OUTER_BOUND('',#5118,.T.);
#3361=FACE_OUTER_BOUND('',#5119,.T.);
#3362=FACE_OUTER_BOUND('',#5120,.T.);
#3363=FACE_OUTER_BOUND('',#5121,.T.);
#3364=FACE_OUTER_BOUND('',#5122,.T.);
#3365=FACE_OUTER_BOUND('',#5123,.T.);
#3366=FACE_OUTER_BOUND('',#5124,.T.);
#3367=FACE_OUTER_BOUND('',#5125,.T.);
#3368=FACE_OUTER_BOUND('',#5126,.T.);
#3369=FACE_OUTER_BOUND('',#5127,.T.);
#3370=FACE_OUTER_BOUND('',#5128,.T.);
#3371=FACE_OUTER_BOUND('',#5129,.T.);
#3372=FACE_OUTER_BOUND('',#5130,.T.);
#3373=FACE_OUTER_BOUND('',#5131,.T.);
#3374=FACE_OUTER_BOUND('',#5132,.T.);
#3375=FACE_OUTER_BOUND('',#5133,.T.);
#5100=EDGE_LOOP('',(#20976,#20977,#20978,#20979));
#5101=EDGE_LOOP('',(#20980,#20981,#20982,#20983,#20984,#20985,#20986,#20987,
#20988,#20989,#20990,#20991,#20992,#20993,#20994,#20995));
#5102=EDGE_LOOP('',(#20996));
#5103=EDGE_LOOP('',(#20997));
#5104=EDGE_LOOP('',(#20998,#20999,#21000,#21001));
#5105=EDGE_LOOP('',(#21002,#21003,#21004,#21005));
#5106=EDGE_LOOP('',(#21006,#21007,#21008,#21009));
#5107=EDGE_LOOP('',(#21010,#21011,#21012));
#5108=EDGE_LOOP('',(#21013,#21014,#21015));
#5109=EDGE_LOOP('',(#21016,#21017,#21018,#21019));
#5110=EDGE_LOOP('',(#21020,#21021,#21022,#21023,#21024,#21025,#21026,#21027,
#21028,#21029,#21030,#21031,#21032,#21033,#21034,#21035));
#5111=EDGE_LOOP('',(#21036));
#5112=EDGE_LOOP('',(#21037));
#5113=EDGE_LOOP('',(#21038,#21039,#21040,#21041));
#5114=EDGE_LOOP('',(#21042,#21043,#21044,#21045));
#5115=EDGE_LOOP('',(#21046,#21047,#21048,#21049));
#5116=EDGE_LOOP('',(#21050,#21051,#21052));
#5117=EDGE_LOOP('',(#21053,#21054,#21055));
#5118=EDGE_LOOP('',(#21056,#21057,#21058,#21059));
#5119=EDGE_LOOP('',(#21060,#21061,#21062,#21063));
#5120=EDGE_LOOP('',(#21064,#21065,#21066,#21067));
#5121=EDGE_LOOP('',(#21068,#21069,#21070,#21071));
#5122=EDGE_LOOP('',(#21072,#21073,#21074,#21075));
#5123=EDGE_LOOP('',(#21076,#21077,#21078,#21079));
#5124=EDGE_LOOP('',(#21080,#21081,#21082,#21083));
#5125=EDGE_LOOP('',(#21084,#21085,#21086,#21087));
#5126=EDGE_LOOP('',(#21088,#21089,#21090,#21091));
#5127=EDGE_LOOP('',(#21092,#21093,#21094,#21095));
#5128=EDGE_LOOP('',(#21096,#21097,#21098,#21099));
#5129=EDGE_LOOP('',(#21100,#21101,#21102,#21103));
#5130=EDGE_LOOP('',(#21104,#21105,#21106,#21107));
#5131=EDGE_LOOP('',(#21108,#21109,#21110,#21111));
#5132=EDGE_LOOP('',(#21112,#21113,#21114,#21115));
#5133=EDGE_LOOP('',(#21116,#21117,#21118,#21119));
#7070=LINE('',#41051,#9907);
#7071=LINE('',#41056,#9908);
#7072=LINE('',#41058,#9909);
#7073=LINE('',#41060,#9910);
#7074=LINE('',#41062,#9911);
#7075=LINE('',#41064,#9912);
#7076=LINE('',#41066,#9913);
#7077=LINE('',#41068,#9914);
#7078=LINE('',#41070,#9915);
#7079=LINE('',#41072,#9916);
#7080=LINE('',#41074,#9917);
#7081=LINE('',#41076,#9918);
#7082=LINE('',#41078,#9919);
#7083=LINE('',#41080,#9920);
#7084=LINE('',#41082,#9921);
#7085=LINE('',#41084,#9922);
#7086=LINE('',#41085,#9923);
#7087=LINE('',#41090,#9924);
#7088=LINE('',#41095,#9925);
#7089=LINE('',#41098,#9926);
#7090=LINE('',#41102,#9927);
#7091=LINE('',#41105,#9928);
#7092=LINE('',#41110,#9929);
#7093=LINE('',#41115,#9930);
#7094=LINE('',#41117,#9931);
#7095=LINE('',#41119,#9932);
#7096=LINE('',#41121,#9933);
#7097=LINE('',#41123,#9934);
#7098=LINE('',#41125,#9935);
#7099=LINE('',#41127,#9936);
#7100=LINE('',#41129,#9937);
#7101=LINE('',#41131,#9938);
#7102=LINE('',#41133,#9939);
#7103=LINE('',#41135,#9940);
#7104=LINE('',#41137,#9941);
#7105=LINE('',#41139,#9942);
#7106=LINE('',#41141,#9943);
#7107=LINE('',#41143,#9944);
#7108=LINE('',#41144,#9945);
#7109=LINE('',#41149,#9946);
#7110=LINE('',#41154,#9947);
#7111=LINE('',#41157,#9948);
#7112=LINE('',#41161,#9949);
#7113=LINE('',#41164,#9950);
#7114=LINE('',#41166,#9951);
#7115=LINE('',#41167,#9952);
#7116=LINE('',#41169,#9953);
#7117=LINE('',#41171,#9954);
#7118=LINE('',#41172,#9955);
#7119=LINE('',#41174,#9956);
#7120=LINE('',#41176,#9957);
#7121=LINE('',#41178,#9958);
#7122=LINE('',#41179,#9959);
#7123=LINE('',#41181,#9960);
#7124=LINE('',#41183,#9961);
#7125=LINE('',#41185,#9962);
#7126=LINE('',#41189,#9963);
#7127=LINE('',#41191,#9964);
#7128=LINE('',#41193,#9965);
#7129=LINE('',#41195,#9966);
#9907=VECTOR('',#34232,1.65);
#9908=VECTOR('',#34237,10.);
#9909=VECTOR('',#34238,10.);
#9910=VECTOR('',#34239,10.);
#9911=VECTOR('',#34240,10.);
#9912=VECTOR('',#34241,10.);
#9913=VECTOR('',#34242,10.);
#9914=VECTOR('',#34243,10.);
#9915=VECTOR('',#34244,10.);
#9916=VECTOR('',#34245,9.99999999999998);
#9917=VECTOR('',#34246,10.);
#9918=VECTOR('',#34247,9.99999999999998);
#9919=VECTOR('',#34248,10.);
#9920=VECTOR('',#34249,10.);
#9921=VECTOR('',#34250,10.);
#9922=VECTOR('',#34251,9.99999999999998);
#9923=VECTOR('',#34252,10.);
#9924=VECTOR('',#34257,1.55);
#9925=VECTOR('',#34264,1.65);
#9926=VECTOR('',#34267,1.55);
#9927=VECTOR('',#34272,1.55);
#9928=VECTOR('',#34275,1.55);
#9929=VECTOR('',#34280,1.65);
#9930=VECTOR('',#34285,10.);
#9931=VECTOR('',#34286,10.);
#9932=VECTOR('',#34287,9.99999999999998);
#9933=VECTOR('',#34288,10.);
#9934=VECTOR('',#34289,10.);
#9935=VECTOR('',#34290,10.);
#9936=VECTOR('',#34291,9.99999999999998);
#9937=VECTOR('',#34292,10.);
#9938=VECTOR('',#34293,9.99999999999998);
#9939=VECTOR('',#34294,10.);
#9940=VECTOR('',#34295,10.);
#9941=VECTOR('',#34296,10.);
#9942=VECTOR('',#34297,10.);
#9943=VECTOR('',#34298,10.);
#9944=VECTOR('',#34299,10.);
#9945=VECTOR('',#34300,10.);
#9946=VECTOR('',#34305,1.55);
#9947=VECTOR('',#34312,1.65);
#9948=VECTOR('',#34315,1.55);
#9949=VECTOR('',#34320,0.775000000000001);
#9950=VECTOR('',#34323,0.775);
#9951=VECTOR('',#34326,10.);
#9952=VECTOR('',#34327,10.);
#9953=VECTOR('',#34330,10.);
#9954=VECTOR('',#34333,10.);
#9955=VECTOR('',#34334,10.);
#9956=VECTOR('',#34337,10.);
#9957=VECTOR('',#34340,10.);
#9958=VECTOR('',#34343,10.);
#9959=VECTOR('',#34344,10.);
#9960=VECTOR('',#34347,10.);
#9961=VECTOR('',#34350,10.);
#9962=VECTOR('',#34353,10.);
#9963=VECTOR('',#34360,10.);
#9964=VECTOR('',#34363,10.);
#9965=VECTOR('',#34366,10.);
#9966=VECTOR('',#34369,10.);
#12744=CIRCLE('',#32235,1.55);
#12745=CIRCLE('',#32236,1.75);
#12746=CIRCLE('',#32238,1.75);
#12747=CIRCLE('',#32240,1.55);
#12748=CIRCLE('',#32242,1.55);
#12749=CIRCLE('',#32244,1.55);
#12750=CIRCLE('',#32248,1.55);
#12751=CIRCLE('',#32249,1.75);
#12752=CIRCLE('',#32251,1.75);
#12753=CIRCLE('',#32253,1.55);
#12754=CIRCLE('',#32255,1.55);
#12755=CIRCLE('',#32257,1.55);
#13244=VERTEX_POINT('',#41048);
#13245=VERTEX_POINT('',#41050);
#13246=VERTEX_POINT('',#41054);
#13247=VERTEX_POINT('',#41055);
#13248=VERTEX_POINT('',#41057);
#13249=VERTEX_POINT('',#41059);
#13250=VERTEX_POINT('',#41061);
#13251=VERTEX_POINT('',#41063);
#13252=VERTEX_POINT('',#41065);
#13253=VERTEX_POINT('',#41067);
#13254=VERTEX_POINT('',#41069);
#13255=VERTEX_POINT('',#41071);
#13256=VERTEX_POINT('',#41073);
#13257=VERTEX_POINT('',#41075);
#13258=VERTEX_POINT('',#41077);
#13259=VERTEX_POINT('',#41079);
#13260=VERTEX_POINT('',#41081);
#13261=VERTEX_POINT('',#41083);
#13262=VERTEX_POINT('',#41086);
#13263=VERTEX_POINT('',#41089);
#13264=VERTEX_POINT('',#41093);
#13265=VERTEX_POINT('',#41097);
#13266=VERTEX_POINT('',#41101);
#13267=VERTEX_POINT('',#41104);
#13268=VERTEX_POINT('',#41107);
#13269=VERTEX_POINT('',#41109);
#13270=VERTEX_POINT('',#41113);
#13271=VERTEX_POINT('',#41114);
#13272=VERTEX_POINT('',#41116);
#13273=VERTEX_POINT('',#41118);
#13274=VERTEX_POINT('',#41120);
#13275=VERTEX_POINT('',#41122);
#13276=VERTEX_POINT('',#41124);
#13277=VERTEX_POINT('',#41126);
#13278=VERTEX_POINT('',#41128);
#13279=VERTEX_POINT('',#41130);
#13280=VERTEX_POINT('',#41132);
#13281=VERTEX_POINT('',#41134);
#13282=VERTEX_POINT('',#41136);
#13283=VERTEX_POINT('',#41138);
#13284=VERTEX_POINT('',#41140);
#13285=VERTEX_POINT('',#41142);
#13286=VERTEX_POINT('',#41145);
#13287=VERTEX_POINT('',#41148);
#13288=VERTEX_POINT('',#41152);
#13289=VERTEX_POINT('',#41156);
#13290=VERTEX_POINT('',#41160);
#13291=VERTEX_POINT('',#41163);
#16339=EDGE_CURVE('',#13244,#13244,#12744,.T.);
#16340=EDGE_CURVE('',#13244,#13245,#7070,.T.);
#16341=EDGE_CURVE('',#13245,#13245,#12745,.T.);
#16342=EDGE_CURVE('',#13246,#13247,#7071,.T.);
#16343=EDGE_CURVE('',#13246,#13248,#7072,.T.);
#16344=EDGE_CURVE('',#13248,#13249,#7073,.T.);
#16345=EDGE_CURVE('',#13249,#13250,#7074,.T.);
#16346=EDGE_CURVE('',#13250,#13251,#7075,.T.);
#16347=EDGE_CURVE('',#13251,#13252,#7076,.T.);
#16348=EDGE_CURVE('',#13253,#13252,#7077,.T.);
#16349=EDGE_CURVE('',#13253,#13254,#7078,.T.);
#16350=EDGE_CURVE('',#13255,#13254,#7079,.T.);
#16351=EDGE_CURVE('',#13255,#13256,#7080,.T.);
#16352=EDGE_CURVE('',#13257,#13256,#7081,.T.);
#16353=EDGE_CURVE('',#13257,#13258,#7082,.T.);
#16354=EDGE_CURVE('',#13259,#13258,#7083,.T.);
#16355=EDGE_CURVE('',#13259,#13260,#7084,.T.);
#16356=EDGE_CURVE('',#13261,#13260,#7085,.T.);
#16357=EDGE_CURVE('',#13261,#13247,#7086,.T.);
#16358=EDGE_CURVE('',#13262,#13262,#12746,.T.);
#16359=EDGE_CURVE('',#13244,#13263,#7087,.T.);
#16360=EDGE_CURVE('',#13263,#13263,#12747,.T.);
#16361=EDGE_CURVE('',#13264,#13264,#12748,.T.);
#16362=EDGE_CURVE('',#13264,#13262,#7088,.T.);
#16363=EDGE_CURVE('',#13264,#13265,#7089,.T.);
#16364=EDGE_CURVE('',#13265,#13265,#12749,.T.);
#16365=EDGE_CURVE('',#13266,#13263,#7090,.T.);
#16366=EDGE_CURVE('',#13267,#13265,#7091,.T.);
#16367=EDGE_CURVE('',#13268,#13268,#12750,.T.);
#16368=EDGE_CURVE('',#13268,#13269,#7092,.T.);
#16369=EDGE_CURVE('',#13269,#13269,#12751,.T.);
#16370=EDGE_CURVE('',#13270,#13271,#7093,.T.);
#16371=EDGE_CURVE('',#13270,#13272,#7094,.T.);
#16372=EDGE_CURVE('',#13273,#13272,#7095,.T.);
#16373=EDGE_CURVE('',#13273,#13274,#7096,.T.);
#16374=EDGE_CURVE('',#13275,#13274,#7097,.T.);
#16375=EDGE_CURVE('',#13275,#13276,#7098,.T.);
#16376=EDGE_CURVE('',#13277,#13276,#7099,.T.);
#16377=EDGE_CURVE('',#13277,#13278,#7100,.T.);
#16378=EDGE_CURVE('',#13279,#13278,#7101,.T.);
#16379=EDGE_CURVE('',#13279,#13280,#7102,.T.);
#16380=EDGE_CURVE('',#13281,#13280,#7103,.T.);
#16381=EDGE_CURVE('',#13281,#13282,#7104,.T.);
#16382=EDGE_CURVE('',#13282,#13283,#7105,.T.);
#16383=EDGE_CURVE('',#13283,#13284,#7106,.T.);
#16384=EDGE_CURVE('',#13284,#13285,#7107,.T.);
#16385=EDGE_CURVE('',#13285,#13271,#7108,.T.);
#16386=EDGE_CURVE('',#13286,#13286,#12752,.T.);
#16387=EDGE_CURVE('',#13268,#13287,#7109,.T.);
#16388=EDGE_CURVE('',#13287,#13287,#12753,.T.);
#16389=EDGE_CURVE('',#13288,#13288,#12754,.T.);
#16390=EDGE_CURVE('',#13288,#13286,#7110,.T.);
#16391=EDGE_CURVE('',#13288,#13289,#7111,.T.);
#16392=EDGE_CURVE('',#13289,#13289,#12755,.T.);
#16393=EDGE_CURVE('',#13290,#13287,#7112,.T.);
#16394=EDGE_CURVE('',#13291,#13289,#7113,.T.);
#16395=EDGE_CURVE('',#13247,#13270,#7114,.T.);
#16396=EDGE_CURVE('',#13271,#13246,#7115,.T.);
#16397=EDGE_CURVE('',#13272,#13261,#7116,.T.);
#16398=EDGE_CURVE('',#13252,#13281,#7117,.T.);
#16399=EDGE_CURVE('',#13280,#13253,#7118,.T.);
#16400=EDGE_CURVE('',#13254,#13279,#7119,.T.);
#16401=EDGE_CURVE('',#13278,#13255,#7120,.T.);
#16402=EDGE_CURVE('',#13256,#13277,#7121,.T.);
#16403=EDGE_CURVE('',#13276,#13257,#7122,.T.);
#16404=EDGE_CURVE('',#13258,#13275,#7123,.T.);
#16405=EDGE_CURVE('',#13274,#13259,#7124,.T.);
#16406=EDGE_CURVE('',#13260,#13273,#7125,.T.);
#16407=EDGE_CURVE('',#13282,#13251,#7126,.T.);
#16408=EDGE_CURVE('',#13283,#13250,#7127,.T.);
#16409=EDGE_CURVE('',#13284,#13249,#7128,.T.);
#16410=EDGE_CURVE('',#13285,#13248,#7129,.T.);
#20976=ORIENTED_EDGE('',*,*,#16339,.T.);
#20977=ORIENTED_EDGE('',*,*,#16340,.T.);
#20978=ORIENTED_EDGE('',*,*,#16341,.T.);
#20979=ORIENTED_EDGE('',*,*,#16340,.F.);
#20980=ORIENTED_EDGE('',*,*,#16342,.F.);
#20981=ORIENTED_EDGE('',*,*,#16343,.T.);
#20982=ORIENTED_EDGE('',*,*,#16344,.T.);
#20983=ORIENTED_EDGE('',*,*,#16345,.T.);
#20984=ORIENTED_EDGE('',*,*,#16346,.T.);
#20985=ORIENTED_EDGE('',*,*,#16347,.T.);
#20986=ORIENTED_EDGE('',*,*,#16348,.F.);
#20987=ORIENTED_EDGE('',*,*,#16349,.T.);
#20988=ORIENTED_EDGE('',*,*,#16350,.F.);
#20989=ORIENTED_EDGE('',*,*,#16351,.T.);
#20990=ORIENTED_EDGE('',*,*,#16352,.F.);
#20991=ORIENTED_EDGE('',*,*,#16353,.T.);
#20992=ORIENTED_EDGE('',*,*,#16354,.F.);
#20993=ORIENTED_EDGE('',*,*,#16355,.T.);
#20994=ORIENTED_EDGE('',*,*,#16356,.F.);
#20995=ORIENTED_EDGE('',*,*,#16357,.T.);
#20996=ORIENTED_EDGE('',*,*,#16358,.F.);
#20997=ORIENTED_EDGE('',*,*,#16341,.F.);
#20998=ORIENTED_EDGE('',*,*,#16339,.F.);
#20999=ORIENTED_EDGE('',*,*,#16359,.T.);
#21000=ORIENTED_EDGE('',*,*,#16360,.T.);
#21001=ORIENTED_EDGE('',*,*,#16359,.F.);
#21002=ORIENTED_EDGE('',*,*,#16361,.T.);
#21003=ORIENTED_EDGE('',*,*,#16362,.T.);
#21004=ORIENTED_EDGE('',*,*,#16358,.T.);
#21005=ORIENTED_EDGE('',*,*,#16362,.F.);
#21006=ORIENTED_EDGE('',*,*,#16361,.F.);
#21007=ORIENTED_EDGE('',*,*,#16363,.T.);
#21008=ORIENTED_EDGE('',*,*,#16364,.T.);
#21009=ORIENTED_EDGE('',*,*,#16363,.F.);
#21010=ORIENTED_EDGE('',*,*,#16365,.T.);
#21011=ORIENTED_EDGE('',*,*,#16360,.F.);
#21012=ORIENTED_EDGE('',*,*,#16365,.F.);
#21013=ORIENTED_EDGE('',*,*,#16366,.T.);
#21014=ORIENTED_EDGE('',*,*,#16364,.F.);
#21015=ORIENTED_EDGE('',*,*,#16366,.F.);
#21016=ORIENTED_EDGE('',*,*,#16367,.T.);
#21017=ORIENTED_EDGE('',*,*,#16368,.T.);
#21018=ORIENTED_EDGE('',*,*,#16369,.T.);
#21019=ORIENTED_EDGE('',*,*,#16368,.F.);
#21020=ORIENTED_EDGE('',*,*,#16370,.F.);
#21021=ORIENTED_EDGE('',*,*,#16371,.T.);
#21022=ORIENTED_EDGE('',*,*,#16372,.F.);
#21023=ORIENTED_EDGE('',*,*,#16373,.T.);
#21024=ORIENTED_EDGE('',*,*,#16374,.F.);
#21025=ORIENTED_EDGE('',*,*,#16375,.T.);
#21026=ORIENTED_EDGE('',*,*,#16376,.F.);
#21027=ORIENTED_EDGE('',*,*,#16377,.T.);
#21028=ORIENTED_EDGE('',*,*,#16378,.F.);
#21029=ORIENTED_EDGE('',*,*,#16379,.T.);
#21030=ORIENTED_EDGE('',*,*,#16380,.F.);
#21031=ORIENTED_EDGE('',*,*,#16381,.T.);
#21032=ORIENTED_EDGE('',*,*,#16382,.T.);
#21033=ORIENTED_EDGE('',*,*,#16383,.T.);
#21034=ORIENTED_EDGE('',*,*,#16384,.T.);
#21035=ORIENTED_EDGE('',*,*,#16385,.T.);
#21036=ORIENTED_EDGE('',*,*,#16386,.F.);
#21037=ORIENTED_EDGE('',*,*,#16369,.F.);
#21038=ORIENTED_EDGE('',*,*,#16367,.F.);
#21039=ORIENTED_EDGE('',*,*,#16387,.T.);
#21040=ORIENTED_EDGE('',*,*,#16388,.T.);
#21041=ORIENTED_EDGE('',*,*,#16387,.F.);
#21042=ORIENTED_EDGE('',*,*,#16389,.T.);
#21043=ORIENTED_EDGE('',*,*,#16390,.T.);
#21044=ORIENTED_EDGE('',*,*,#16386,.T.);
#21045=ORIENTED_EDGE('',*,*,#16390,.F.);
#21046=ORIENTED_EDGE('',*,*,#16389,.F.);
#21047=ORIENTED_EDGE('',*,*,#16391,.T.);
#21048=ORIENTED_EDGE('',*,*,#16392,.T.);
#21049=ORIENTED_EDGE('',*,*,#16391,.F.);
#21050=ORIENTED_EDGE('',*,*,#16393,.T.);
#21051=ORIENTED_EDGE('',*,*,#16388,.F.);
#21052=ORIENTED_EDGE('',*,*,#16393,.F.);
#21053=ORIENTED_EDGE('',*,*,#16394,.T.);
#21054=ORIENTED_EDGE('',*,*,#16392,.F.);
#21055=ORIENTED_EDGE('',*,*,#16394,.F.);
#21056=ORIENTED_EDGE('',*,*,#16342,.T.);
#21057=ORIENTED_EDGE('',*,*,#16395,.T.);
#21058=ORIENTED_EDGE('',*,*,#16370,.T.);
#21059=ORIENTED_EDGE('',*,*,#16396,.T.);
#21060=ORIENTED_EDGE('',*,*,#16395,.F.);
#21061=ORIENTED_EDGE('',*,*,#16357,.F.);
#21062=ORIENTED_EDGE('',*,*,#16397,.F.);
#21063=ORIENTED_EDGE('',*,*,#16371,.F.);
#21064=ORIENTED_EDGE('',*,*,#16348,.T.);
#21065=ORIENTED_EDGE('',*,*,#16398,.T.);
#21066=ORIENTED_EDGE('',*,*,#16380,.T.);
#21067=ORIENTED_EDGE('',*,*,#16399,.T.);
#21068=ORIENTED_EDGE('',*,*,#16399,.F.);
#21069=ORIENTED_EDGE('',*,*,#16379,.F.);
#21070=ORIENTED_EDGE('',*,*,#16400,.F.);
#21071=ORIENTED_EDGE('',*,*,#16349,.F.);
#21072=ORIENTED_EDGE('',*,*,#16350,.T.);
#21073=ORIENTED_EDGE('',*,*,#16400,.T.);
#21074=ORIENTED_EDGE('',*,*,#16378,.T.);
#21075=ORIENTED_EDGE('',*,*,#16401,.T.);
#21076=ORIENTED_EDGE('',*,*,#16352,.T.);
#21077=ORIENTED_EDGE('',*,*,#16402,.T.);
#21078=ORIENTED_EDGE('',*,*,#16376,.T.);
#21079=ORIENTED_EDGE('',*,*,#16403,.T.);
#21080=ORIENTED_EDGE('',*,*,#16403,.F.);
#21081=ORIENTED_EDGE('',*,*,#16375,.F.);
#21082=ORIENTED_EDGE('',*,*,#16404,.F.);
#21083=ORIENTED_EDGE('',*,*,#16353,.F.);
#21084=ORIENTED_EDGE('',*,*,#16354,.T.);
#21085=ORIENTED_EDGE('',*,*,#16404,.T.);
#21086=ORIENTED_EDGE('',*,*,#16374,.T.);
#21087=ORIENTED_EDGE('',*,*,#16405,.T.);
#21088=ORIENTED_EDGE('',*,*,#16356,.T.);
#21089=ORIENTED_EDGE('',*,*,#16406,.T.);
#21090=ORIENTED_EDGE('',*,*,#16372,.T.);
#21091=ORIENTED_EDGE('',*,*,#16397,.T.);
#21092=ORIENTED_EDGE('',*,*,#16405,.F.);
#21093=ORIENTED_EDGE('',*,*,#16373,.F.);
#21094=ORIENTED_EDGE('',*,*,#16406,.F.);
#21095=ORIENTED_EDGE('',*,*,#16355,.F.);
#21096=ORIENTED_EDGE('',*,*,#16401,.F.);
#21097=ORIENTED_EDGE('',*,*,#16377,.F.);
#21098=ORIENTED_EDGE('',*,*,#16402,.F.);
#21099=ORIENTED_EDGE('',*,*,#16351,.F.);
#21100=ORIENTED_EDGE('',*,*,#16398,.F.);
#21101=ORIENTED_EDGE('',*,*,#16347,.F.);
#21102=ORIENTED_EDGE('',*,*,#16407,.F.);
#21103=ORIENTED_EDGE('',*,*,#16381,.F.);
#21104=ORIENTED_EDGE('',*,*,#16382,.F.);
#21105=ORIENTED_EDGE('',*,*,#16407,.T.);
#21106=ORIENTED_EDGE('',*,*,#16346,.F.);
#21107=ORIENTED_EDGE('',*,*,#16408,.F.);
#21108=ORIENTED_EDGE('',*,*,#16383,.F.);
#21109=ORIENTED_EDGE('',*,*,#16408,.T.);
#21110=ORIENTED_EDGE('',*,*,#16345,.F.);
#21111=ORIENTED_EDGE('',*,*,#16409,.F.);
#21112=ORIENTED_EDGE('',*,*,#16384,.F.);
#21113=ORIENTED_EDGE('',*,*,#16409,.T.);
#21114=ORIENTED_EDGE('',*,*,#16344,.F.);
#21115=ORIENTED_EDGE('',*,*,#16410,.F.);
#21116=ORIENTED_EDGE('',*,*,#16396,.F.);
#21117=ORIENTED_EDGE('',*,*,#16385,.F.);
#21118=ORIENTED_EDGE('',*,*,#16410,.T.);
#21119=ORIENTED_EDGE('',*,*,#16343,.F.);
#30250=CONICAL_SURFACE('',#32234,1.65,0.785398163397459);
#30251=CONICAL_SURFACE('',#32241,1.65,0.785398163397459);
#30252=CONICAL_SURFACE('',#32245,1.55,1.02974425867666);
#30253=CONICAL_SURFACE('',#32246,1.55,1.02974425867666);
#30254=CONICAL_SURFACE('',#32247,1.65,0.785398163397448);
#30255=CONICAL_SURFACE('',#32254,1.65,0.785398163397448);
#30256=CONICAL_SURFACE('',#32258,0.775000000000001,1.02974425867665);
#30257=CONICAL_SURFACE('',#32259,0.775,1.02974425867665);
#30321=ADVANCED_FACE('',(#3346),#30250,.F.);
#30322=ADVANCED_FACE('',(#3347,#2016,#2017),#2232,.T.);
#30323=ADVANCED_FACE('',(#3348),#1765,.F.);
#30324=ADVANCED_FACE('',(#3349),#30251,.F.);
#30325=ADVANCED_FACE('',(#3350),#1766,.F.);
#30326=ADVANCED_FACE('',(#3351),#30252,.F.);
#30327=ADVANCED_FACE('',(#3352),#30253,.F.);
#30328=ADVANCED_FACE('',(#3353),#30254,.F.);
#30329=ADVANCED_FACE('',(#3354,#2018,#2019),#2233,.F.);
#30330=ADVANCED_FACE('',(#3355),#1767,.F.);
#30331=ADVANCED_FACE('',(#3356),#30255,.F.);
#30332=ADVANCED_FACE('',(#3357),#1768,.F.);
#30333=ADVANCED_FACE('',(#3358),#30256,.F.);
#30334=ADVANCED_FACE('',(#3359),#30257,.F.);
#30335=ADVANCED_FACE('',(#3360),#2234,.T.);
#30336=ADVANCED_FACE('',(#3361),#2235,.T.);
#30337=ADVANCED_FACE('',(#3362),#2236,.T.);
#30338=ADVANCED_FACE('',(#3363),#2237,.T.);
#30339=ADVANCED_FACE('',(#3364),#2238,.T.);
#30340=ADVANCED_FACE('',(#3365),#2239,.T.);
#30341=ADVANCED_FACE('',(#3366),#2240,.T.);
#30342=ADVANCED_FACE('',(#3367),#2241,.T.);
#30343=ADVANCED_FACE('',(#3368),#2242,.T.);
#30344=ADVANCED_FACE('',(#3369),#2243,.T.);
#30345=ADVANCED_FACE('',(#3370),#2244,.T.);
#30346=ADVANCED_FACE('',(#3371),#2245,.T.);
#30347=ADVANCED_FACE('',(#3372),#2246,.T.);
#30348=ADVANCED_FACE('',(#3373),#2247,.T.);
#30349=ADVANCED_FACE('',(#3374),#2248,.T.);
#30350=ADVANCED_FACE('',(#3375),#2249,.T.);
#32075=CLOSED_SHELL('',(#30321,#30322,#30323,#30324,#30325,#30326,#30327,
#30328,#30329,#30330,#30331,#30332,#30333,#30334,#30335,#30336,#30337,#30338,
#30339,#30340,#30341,#30342,#30343,#30344,#30345,#30346,#30347,#30348,#30349,
#30350));
#32233=AXIS2_PLACEMENT_3D('',#41046,#34226,#34227);
#32234=AXIS2_PLACEMENT_3D('',#41047,#34228,#34229);
#32235=AXIS2_PLACEMENT_3D('',#41049,#34230,#34231);
#32236=AXIS2_PLACEMENT_3D('',#41052,#34233,#34234);
#32237=AXIS2_PLACEMENT_3D('',#41053,#34235,#34236);
#32238=AXIS2_PLACEMENT_3D('',#41087,#34253,#34254);
#32239=AXIS2_PLACEMENT_3D('',#41088,#34255,#34256);
#32240=AXIS2_PLACEMENT_3D('',#41091,#34258,#34259);
#32241=AXIS2_PLACEMENT_3D('',#41092,#34260,#34261);
#32242=AXIS2_PLACEMENT_3D('',#41094,#34262,#34263);
#32243=AXIS2_PLACEMENT_3D('',#41096,#34265,#34266);
#32244=AXIS2_PLACEMENT_3D('',#41099,#34268,#34269);
#32245=AXIS2_PLACEMENT_3D('',#41100,#34270,#34271);
#32246=AXIS2_PLACEMENT_3D('',#41103,#34273,#34274);
#32247=AXIS2_PLACEMENT_3D('',#41106,#34276,#34277);
#32248=AXIS2_PLACEMENT_3D('',#41108,#34278,#34279);
#32249=AXIS2_PLACEMENT_3D('',#41111,#34281,#34282);
#32250=AXIS2_PLACEMENT_3D('',#41112,#34283,#34284);
#32251=AXIS2_PLACEMENT_3D('',#41146,#34301,#34302);
#32252=AXIS2_PLACEMENT_3D('',#41147,#34303,#34304);
#32253=AXIS2_PLACEMENT_3D('',#41150,#34306,#34307);
#32254=AXIS2_PLACEMENT_3D('',#41151,#34308,#34309);
#32255=AXIS2_PLACEMENT_3D('',#41153,#34310,#34311);
#32256=AXIS2_PLACEMENT_3D('',#41155,#34313,#34314);
#32257=AXIS2_PLACEMENT_3D('',#41158,#34316,#34317);
#32258=AXIS2_PLACEMENT_3D('',#41159,#34318,#34319);
#32259=AXIS2_PLACEMENT_3D('',#41162,#34321,#34322);
#32260=AXIS2_PLACEMENT_3D('',#41165,#34324,#34325);
#32261=AXIS2_PLACEMENT_3D('',#41168,#34328,#34329);
#32262=AXIS2_PLACEMENT_3D('',#41170,#34331,#34332);
#32263=AXIS2_PLACEMENT_3D('',#41173,#34335,#34336);
#32264=AXIS2_PLACEMENT_3D('',#41175,#34338,#34339);
#32265=AXIS2_PLACEMENT_3D('',#41177,#34341,#34342);
#32266=AXIS2_PLACEMENT_3D('',#41180,#34345,#34346);
#32267=AXIS2_PLACEMENT_3D('',#41182,#34348,#34349);
#32268=AXIS2_PLACEMENT_3D('',#41184,#34351,#34352);
#32269=AXIS2_PLACEMENT_3D('',#41186,#34354,#34355);
#32270=AXIS2_PLACEMENT_3D('',#41187,#34356,#34357);
#32271=AXIS2_PLACEMENT_3D('',#41188,#34358,#34359);
#32272=AXIS2_PLACEMENT_3D('',#41190,#34361,#34362);
#32273=AXIS2_PLACEMENT_3D('',#41192,#34364,#34365);
#32274=AXIS2_PLACEMENT_3D('',#41194,#34367,#34368);
#32275=AXIS2_PLACEMENT_3D('',#41196,#34370,#34371);
#34226=DIRECTION('axis',(0.,0.,1.));
#34227=DIRECTION('refdir',(1.,0.,0.));
#34228=DIRECTION('center_axis',(0.,1.,0.));
#34229=DIRECTION('ref_axis',(1.,0.,0.));
#34230=DIRECTION('center_axis',(0.,-1.,0.));
#34231=DIRECTION('ref_axis',(1.,0.,0.));
#34232=DIRECTION('',(-0.707106781186555,0.70710678118654,8.65956056235503E-17));
#34233=DIRECTION('center_axis',(0.,1.,0.));
#34234=DIRECTION('ref_axis',(1.,0.,0.));
#34235=DIRECTION('center_axis',(0.,1.,0.));
#34236=DIRECTION('ref_axis',(0.,0.,1.));
#34237=DIRECTION('',(-0.499999999999999,0.,0.866025403784439));
#34238=DIRECTION('',(-0.5,0.,-0.866025403784439));
#34239=DIRECTION('',(0.,0.,-1.));
#34240=DIRECTION('',(1.,0.,0.));
#34241=DIRECTION('',(0.,0.,1.));
#34242=DIRECTION('',(-0.5,0.,0.866025403784439));
#34243=DIRECTION('',(-0.500000000000003,0.,-0.866025403784437));
#34244=DIRECTION('',(1.,0.,0.));
#34245=DIRECTION('',(-0.707106781186548,0.,0.707106781186548));
#34246=DIRECTION('',(0.,0.,-1.));
#34247=DIRECTION('',(0.707106781186548,0.,0.707106781186548));
#34248=DIRECTION('',(-1.,0.,0.));
#34249=DIRECTION('',(0.707106781186548,0.,-0.707106781186547));
#34250=DIRECTION('',(0.,0.,1.));
#34251=DIRECTION('',(-0.707106781186548,0.,-0.707106781186548));
#34252=DIRECTION('',(1.,0.,0.));
#34253=DIRECTION('center_axis',(0.,1.,0.));
#34254=DIRECTION('ref_axis',(1.,0.,0.));
#34255=DIRECTION('center_axis',(0.,-1.,0.));
#34256=DIRECTION('ref_axis',(1.,0.,0.));
#34257=DIRECTION('',(0.,-1.,0.));
#34258=DIRECTION('center_axis',(0.,-1.,0.));
#34259=DIRECTION('ref_axis',(1.,0.,0.));
#34260=DIRECTION('center_axis',(0.,1.,0.));
#34261=DIRECTION('ref_axis',(1.,0.,0.));
#34262=DIRECTION('center_axis',(0.,-1.,0.));
#34263=DIRECTION('ref_axis',(1.,0.,0.));
#34264=DIRECTION('',(-0.707106781186555,0.70710678118654,8.65956056235503E-17));
#34265=DIRECTION('center_axis',(0.,-1.,0.));
#34266=DIRECTION('ref_axis',(1.,0.,0.));
#34267=DIRECTION('',(0.,-1.,0.));
#34268=DIRECTION('center_axis',(0.,-1.,0.));
#34269=DIRECTION('ref_axis',(1.,0.,0.));
#34270=DIRECTION('center_axis',(0.,1.,0.));
#34271=DIRECTION('ref_axis',(1.,0.,0.));
#34272=DIRECTION('',(-0.857167300702115,0.515038074910049,1.04972719113862E-16));
#34273=DIRECTION('center_axis',(0.,1.,0.));
#34274=DIRECTION('ref_axis',(1.,0.,0.));
#34275=DIRECTION('',(-0.857167300702115,0.515038074910049,1.04972719113862E-16));
#34276=DIRECTION('center_axis',(0.,-1.,0.));
#34277=DIRECTION('ref_axis',(1.,0.,0.));
#34278=DIRECTION('center_axis',(0.,1.,0.));
#34279=DIRECTION('ref_axis',(1.,0.,0.));
#34280=DIRECTION('',(-0.707106781186547,-0.707106781186548,-8.65956056235493E-17));
#34281=DIRECTION('center_axis',(0.,-1.,0.));
#34282=DIRECTION('ref_axis',(1.,0.,0.));
#34283=DIRECTION('center_axis',(0.,1.,0.));
#34284=DIRECTION('ref_axis',(1.,0.,0.));
#34285=DIRECTION('',(0.499999999999999,0.,-0.866025403784439));
#34286=DIRECTION('',(-1.,0.,0.));
#34287=DIRECTION('',(0.707106781186548,0.,0.707106781186548));
#34288=DIRECTION('',(0.,0.,-1.));
#34289=DIRECTION('',(-0.707106781186548,0.,0.707106781186547));
#34290=DIRECTION('',(1.,0.,0.));
#34291=DIRECTION('',(-0.707106781186548,0.,-0.707106781186548));
#34292=DIRECTION('',(0.,0.,1.));
#34293=DIRECTION('',(0.707106781186548,0.,-0.707106781186548));
#34294=DIRECTION('',(-1.,0.,0.));
#34295=DIRECTION('',(0.500000000000003,0.,0.866025403784437));
#34296=DIRECTION('',(0.5,0.,-0.866025403784439));
#34297=DIRECTION('',(0.,0.,-1.));
#34298=DIRECTION('',(-1.,0.,0.));
#34299=DIRECTION('',(0.,0.,1.));
#34300=DIRECTION('',(0.5,0.,0.866025403784439));
#34301=DIRECTION('center_axis',(0.,-1.,0.));
#34302=DIRECTION('ref_axis',(1.,0.,0.));
#34303=DIRECTION('center_axis',(0.,1.,0.));
#34304=DIRECTION('ref_axis',(1.,0.,0.));
#34305=DIRECTION('',(0.,1.,0.));
#34306=DIRECTION('center_axis',(0.,1.,0.));
#34307=DIRECTION('ref_axis',(1.,0.,0.));
#34308=DIRECTION('center_axis',(0.,-1.,0.));
#34309=DIRECTION('ref_axis',(1.,0.,0.));
#34310=DIRECTION('center_axis',(0.,1.,0.));
#34311=DIRECTION('ref_axis',(1.,0.,0.));
#34312=DIRECTION('',(-0.707106781186547,-0.707106781186548,-8.65956056235493E-17));
#34313=DIRECTION('center_axis',(0.,1.,0.));
#34314=DIRECTION('ref_axis',(1.,0.,0.));
#34315=DIRECTION('',(0.,1.,0.));
#34316=DIRECTION('center_axis',(0.,1.,0.));
#34317=DIRECTION('ref_axis',(1.,0.,0.));
#34318=DIRECTION('center_axis',(0.,-1.,0.));
#34319=DIRECTION('ref_axis',(1.,0.,0.));
#34320=DIRECTION('',(-0.85716730070211,-0.515038074910058,-1.04972719113862E-16));
#34321=DIRECTION('center_axis',(0.,-1.,0.));
#34322=DIRECTION('ref_axis',(1.,0.,0.));
#34323=DIRECTION('',(-0.85716730070211,-0.515038074910058,-1.04972719113862E-16));
#34324=DIRECTION('center_axis',(0.866025403784439,0.,0.499999999999999));
#34325=DIRECTION('ref_axis',(0.499999999999999,0.,-0.866025403784439));
#34326=DIRECTION('',(0.,-1.,0.));
#34327=DIRECTION('',(0.,1.,0.));
#34328=DIRECTION('center_axis',(0.,0.,1.));
#34329=DIRECTION('ref_axis',(1.,0.,0.));
#34330=DIRECTION('',(0.,1.,0.));
#34331=DIRECTION('center_axis',(-0.866025403784437,0.,0.500000000000003));
#34332=DIRECTION('ref_axis',(0.500000000000003,0.,0.866025403784437));
#34333=DIRECTION('',(0.,-1.,0.));
#34334=DIRECTION('',(0.,1.,0.));
#34335=DIRECTION('center_axis',(0.,0.,1.));
#34336=DIRECTION('ref_axis',(1.,0.,0.));
#34337=DIRECTION('',(0.,-1.,0.));
#34338=DIRECTION('center_axis',(0.707106781186548,0.,0.707106781186548));
#34339=DIRECTION('ref_axis',(0.707106781186548,0.,-0.707106781186548));
#34340=DIRECTION('',(0.,1.,0.));
#34341=DIRECTION('center_axis',(0.707106781186548,0.,-0.707106781186548));
#34342=DIRECTION('ref_axis',(-0.707106781186548,0.,-0.707106781186548));
#34343=DIRECTION('',(0.,-1.,0.));
#34344=DIRECTION('',(0.,1.,0.));
#34345=DIRECTION('center_axis',(0.,0.,-1.));
#34346=DIRECTION('ref_axis',(-1.,0.,0.));
#34347=DIRECTION('',(0.,-1.,0.));
#34348=DIRECTION('center_axis',(-0.707106781186547,0.,-0.707106781186548));
#34349=DIRECTION('ref_axis',(-0.707106781186548,0.,0.707106781186547));
#34350=DIRECTION('',(0.,1.,0.));
#34351=DIRECTION('center_axis',(-0.707106781186548,0.,0.707106781186548));
#34352=DIRECTION('ref_axis',(0.707106781186548,0.,0.707106781186548));
#34353=DIRECTION('',(0.,-1.,0.));
#34354=DIRECTION('center_axis',(-1.,0.,0.));
#34355=DIRECTION('ref_axis',(0.,0.,1.));
#34356=DIRECTION('center_axis',(1.,0.,0.));
#34357=DIRECTION('ref_axis',(0.,0.,-1.));
#34358=DIRECTION('center_axis',(-0.866025403784439,0.,-0.5));
#34359=DIRECTION('ref_axis',(-0.5,0.,0.866025403784439));
#34360=DIRECTION('',(0.,1.,0.));
#34361=DIRECTION('center_axis',(-1.,0.,0.));
#34362=DIRECTION('ref_axis',(0.,0.,1.));
#34363=DIRECTION('',(0.,1.,0.));
#34364=DIRECTION('center_axis',(0.,0.,1.));
#34365=DIRECTION('ref_axis',(1.,0.,0.));
#34366=DIRECTION('',(0.,1.,0.));
#34367=DIRECTION('center_axis',(1.,0.,0.));
#34368=DIRECTION('ref_axis',(0.,0.,-1.));
#34369=DIRECTION('',(0.,1.,0.));
#34370=DIRECTION('center_axis',(0.866025403784439,0.,-0.5));
#34371=DIRECTION('ref_axis',(-0.5,0.,-0.866025403784439));
#41046=CARTESIAN_POINT('',(0.,0.,0.));
#41047=CARTESIAN_POINT('Origin',(10.,119.9,3.5));
#41048=CARTESIAN_POINT('',(8.45,119.8,3.5));
#41049=CARTESIAN_POINT('Origin',(10.,119.8,3.5));
#41050=CARTESIAN_POINT('',(8.25,120.,3.5));
#41051=CARTESIAN_POINT('',(8.35,119.9,3.5));
#41052=CARTESIAN_POINT('Origin',(10.,120.,3.5));
#41053=CARTESIAN_POINT('Origin',(0.,120.,8.));
#41054=CARTESIAN_POINT('',(-7.6,120.,15.8267949192431));
#41055=CARTESIAN_POINT('',(-7.7,120.,16.));
#41056=CARTESIAN_POINT('',(-4.98044919243113,120.,11.2895998275257));
#41057=CARTESIAN_POINT('',(-10.3867513459481,120.,11.));
#41058=CARTESIAN_POINT('',(-10.3867513459481,120.,11.));
#41059=CARTESIAN_POINT('',(-10.3867513459481,120.,7.));
#41060=CARTESIAN_POINT('',(-10.3867513459481,120.,7.));
#41061=CARTESIAN_POINT('',(10.3867513459481,120.,7.));
#41062=CARTESIAN_POINT('',(10.3867513459481,120.,7.));
#41063=CARTESIAN_POINT('',(10.3867513459481,120.,11.));
#41064=CARTESIAN_POINT('',(10.3867513459481,120.,11.));
#41065=CARTESIAN_POINT('',(7.6,120.,15.8267949192431));
#41066=CARTESIAN_POINT('',(7.5,120.,16.));
#41067=CARTESIAN_POINT('',(7.7,120.,16.));
#41068=CARTESIAN_POINT('',(4.98044919243111,120.,11.2895998275257));
#41069=CARTESIAN_POINT('',(12.1,120.,16.));
#41070=CARTESIAN_POINT('',(12.5,120.,16.));
#41071=CARTESIAN_POINT('',(12.5,120.,15.6));
#41072=CARTESIAN_POINT('',(11.175,120.,16.925));
#41073=CARTESIAN_POINT('',(12.5,120.,0.4));
#41074=CARTESIAN_POINT('',(12.5,120.,0.));
#41075=CARTESIAN_POINT('',(12.1,120.,0.));
#41076=CARTESIAN_POINT('',(11.175,120.,-0.925));
#41077=CARTESIAN_POINT('',(-12.1,120.,0.));
#41078=CARTESIAN_POINT('',(-12.5,120.,0.));
#41079=CARTESIAN_POINT('',(-12.5,120.,0.4));
#41080=CARTESIAN_POINT('',(-11.175,120.,-0.925000000000002));
#41081=CARTESIAN_POINT('',(-12.5,120.,15.6));
#41082=CARTESIAN_POINT('',(-12.5,120.,16.));
#41083=CARTESIAN_POINT('',(-12.1,120.,16.));
#41084=CARTESIAN_POINT('',(-11.175,120.,16.925));
#41085=CARTESIAN_POINT('',(-7.5,120.,16.));
#41086=CARTESIAN_POINT('',(-11.75,120.,3.5));
#41087=CARTESIAN_POINT('Origin',(-10.,120.,3.5));
#41088=CARTESIAN_POINT('Origin',(10.,120.,3.5));
#41089=CARTESIAN_POINT('',(8.45,112.,3.5));
#41090=CARTESIAN_POINT('',(8.45,120.,3.5));
#41091=CARTESIAN_POINT('Origin',(10.,112.,3.5));
#41092=CARTESIAN_POINT('Origin',(-10.,119.9,3.5));
#41093=CARTESIAN_POINT('',(-11.55,119.8,3.5));
#41094=CARTESIAN_POINT('Origin',(-10.,119.8,3.5));
#41095=CARTESIAN_POINT('',(-11.65,119.9,3.5));
#41096=CARTESIAN_POINT('Origin',(-10.,120.,3.5));
#41097=CARTESIAN_POINT('',(-11.55,112.,3.5));
#41098=CARTESIAN_POINT('',(-11.55,120.,3.5));
#41099=CARTESIAN_POINT('Origin',(-10.,112.,3.5));
#41100=CARTESIAN_POINT('Origin',(10.,112.,3.5));
#41101=CARTESIAN_POINT('',(10.,111.068666040507,3.5));
#41102=CARTESIAN_POINT('',(8.45,112.,3.5));
#41103=CARTESIAN_POINT('Origin',(-10.,112.,3.5));
#41104=CARTESIAN_POINT('',(-10.,111.068666040507,3.5));
#41105=CARTESIAN_POINT('',(-11.55,112.,3.5));
#41106=CARTESIAN_POINT('Origin',(10.,20.1,3.5));
#41107=CARTESIAN_POINT('',(8.45,20.2,3.5));
#41108=CARTESIAN_POINT('Origin',(10.,20.2,3.5));
#41109=CARTESIAN_POINT('',(8.25,20.,3.5));
#41110=CARTESIAN_POINT('',(8.35,20.1,3.5));
#41111=CARTESIAN_POINT('Origin',(10.,20.,3.5));
#41112=CARTESIAN_POINT('Origin',(0.,20.,8.));
#41113=CARTESIAN_POINT('',(-7.7,20.,16.));
#41114=CARTESIAN_POINT('',(-7.6,20.,15.8267949192431));
#41115=CARTESIAN_POINT('',(-4.98044919243113,20.,11.2895998275257));
#41116=CARTESIAN_POINT('',(-12.1,20.,16.));
#41117=CARTESIAN_POINT('',(-7.5,20.,16.));
#41118=CARTESIAN_POINT('',(-12.5,20.,15.6));
#41119=CARTESIAN_POINT('',(-11.175,20.,16.925));
#41120=CARTESIAN_POINT('',(-12.5,20.,0.4));
#41121=CARTESIAN_POINT('',(-12.5,20.,16.));
#41122=CARTESIAN_POINT('',(-12.1,20.,0.));
#41123=CARTESIAN_POINT('',(-11.175,20.,-0.925000000000002));
#41124=CARTESIAN_POINT('',(12.1,20.,0.));
#41125=CARTESIAN_POINT('',(-12.5,20.,0.));
#41126=CARTESIAN_POINT('',(12.5,20.,0.4));
#41127=CARTESIAN_POINT('',(11.175,20.,-0.925));
#41128=CARTESIAN_POINT('',(12.5,20.,15.6));
#41129=CARTESIAN_POINT('',(12.5,20.,0.));
#41130=CARTESIAN_POINT('',(12.1,20.,16.));
#41131=CARTESIAN_POINT('',(11.175,20.,16.925));
#41132=CARTESIAN_POINT('',(7.7,20.,16.));
#41133=CARTESIAN_POINT('',(12.5,20.,16.));
#41134=CARTESIAN_POINT('',(7.6,20.,15.8267949192431));
#41135=CARTESIAN_POINT('',(4.98044919243111,20.,11.2895998275257));
#41136=CARTESIAN_POINT('',(10.3867513459481,20.,11.));
#41137=CARTESIAN_POINT('',(7.5,20.,16.));
#41138=CARTESIAN_POINT('',(10.3867513459481,20.,7.));
#41139=CARTESIAN_POINT('',(10.3867513459481,20.,11.));
#41140=CARTESIAN_POINT('',(-10.3867513459481,20.,7.));
#41141=CARTESIAN_POINT('',(10.3867513459481,20.,7.));
#41142=CARTESIAN_POINT('',(-10.3867513459481,20.,11.));
#41143=CARTESIAN_POINT('',(-10.3867513459481,20.,7.));
#41144=CARTESIAN_POINT('',(-10.3867513459481,20.,11.));
#41145=CARTESIAN_POINT('',(-11.75,20.,3.5));
#41146=CARTESIAN_POINT('Origin',(-10.,20.,3.5));
#41147=CARTESIAN_POINT('Origin',(10.,20.,3.5));
#41148=CARTESIAN_POINT('',(8.45,28.,3.5));
#41149=CARTESIAN_POINT('',(8.45,20.,3.5));
#41150=CARTESIAN_POINT('Origin',(10.,28.,3.5));
#41151=CARTESIAN_POINT('Origin',(-10.,20.1,3.5));
#41152=CARTESIAN_POINT('',(-11.55,20.2,3.5));
#41153=CARTESIAN_POINT('Origin',(-10.,20.2,3.5));
#41154=CARTESIAN_POINT('',(-11.65,20.1,3.5));
#41155=CARTESIAN_POINT('Origin',(-10.,20.,3.5));
#41156=CARTESIAN_POINT('',(-11.55,28.,3.5));
#41157=CARTESIAN_POINT('',(-11.55,20.,3.5));
#41158=CARTESIAN_POINT('Origin',(-10.,28.,3.5));
#41159=CARTESIAN_POINT('Origin',(10.,28.4656669797464,3.5));
#41160=CARTESIAN_POINT('',(10.,28.9313339594927,3.5));
#41161=CARTESIAN_POINT('',(9.225,28.4656669797464,3.5));
#41162=CARTESIAN_POINT('Origin',(-10.,28.4656669797464,3.5));
#41163=CARTESIAN_POINT('',(-10.,28.9313339594927,3.5));
#41164=CARTESIAN_POINT('',(-10.775,28.4656669797464,3.5));
#41165=CARTESIAN_POINT('Origin',(-7.65,20.,15.9133974596216));
#41166=CARTESIAN_POINT('',(-7.7,20.,16.));
#41167=CARTESIAN_POINT('',(-7.6,20.,15.8267949192431));
#41168=CARTESIAN_POINT('Origin',(-12.5,20.,16.));
#41169=CARTESIAN_POINT('',(-12.1,20.,16.));
#41170=CARTESIAN_POINT('Origin',(7.65,20.,15.9133974596216));
#41171=CARTESIAN_POINT('',(7.6,20.,15.8267949192431));
#41172=CARTESIAN_POINT('',(7.7,20.,16.));
#41173=CARTESIAN_POINT('Origin',(7.5,20.,16.));
#41174=CARTESIAN_POINT('',(12.1,20.,16.));
#41175=CARTESIAN_POINT('Origin',(12.3,20.,15.8));
#41176=CARTESIAN_POINT('',(12.5,20.,15.6));
#41177=CARTESIAN_POINT('Origin',(12.3,20.,0.2));
#41178=CARTESIAN_POINT('',(12.5,20.,0.4));
#41179=CARTESIAN_POINT('',(12.1,20.,0.));
#41180=CARTESIAN_POINT('Origin',(12.5,20.,0.));
#41181=CARTESIAN_POINT('',(-12.1,20.,0.));
#41182=CARTESIAN_POINT('Origin',(-12.3,20.,0.2));
#41183=CARTESIAN_POINT('',(-12.5,20.,0.4));
#41184=CARTESIAN_POINT('Origin',(-12.3,20.,15.8));
#41185=CARTESIAN_POINT('',(-12.5,20.,15.6));
#41186=CARTESIAN_POINT('Origin',(-12.5,20.,0.));
#41187=CARTESIAN_POINT('Origin',(12.5,20.,16.));
#41188=CARTESIAN_POINT('Origin',(10.3867513459481,20.,11.));
#41189=CARTESIAN_POINT('',(10.3867513459481,20.,11.));
#41190=CARTESIAN_POINT('Origin',(10.3867513459481,20.,7.));
#41191=CARTESIAN_POINT('',(10.3867513459481,20.,7.));
#41192=CARTESIAN_POINT('Origin',(-10.3867513459481,20.,7.));
#41193=CARTESIAN_POINT('',(-10.3867513459481,20.,7.));
#41194=CARTESIAN_POINT('Origin',(-10.3867513459481,20.,11.));
#41195=CARTESIAN_POINT('',(-10.3867513459481,20.,11.));
#41196=CARTESIAN_POINT('Origin',(-7.5,20.,16.));
#135254=UNCERTAINTY_MEASURE_WITH_UNIT(LENGTH_MEASURE(0.01),#135283,
'DISTANCE_ACCURACY_VALUE',
'Maximum model space distance between geometric entities at asserted c
onnectivities');
#135267=UNCERTAINTY_MEASURE_WITH_UNIT(LENGTH_MEASURE(0.01),#135283,
'DISTANCE_ACCURACY_VALUE',
'Maximum model space distance between geometric entities at asserted c
onnectivities');
#135269=(
GEOMETRIC_REPRESENTATION_CONTEXT(3)
GLOBAL_UNCERTAINTY_ASSIGNED_CONTEXT((#135254))
GLOBAL_UNIT_ASSIGNED_CONTEXT((#135283,#135285,#135286))
REPRESENTATION_CONTEXT('','3D')
);
#135282=(
GEOMETRIC_REPRESENTATION_CONTEXT(3)
GLOBAL_UNCERTAINTY_ASSIGNED_CONTEXT((#135267))
GLOBAL_UNIT_ASSIGNED_CONTEXT((#135283,#135285,#135286))
REPRESENTATION_CONTEXT('','3D')
);
#135283=(
LENGTH_UNIT()
NAMED_UNIT(*)
SI_UNIT(.MILLI.,.METRE.)
);
#135285=(
NAMED_UNIT(*)
PLANE_ANGLE_UNIT()
SI_UNIT($,.RADIAN.)
);
#135286=(
NAMED_UNIT(*)
SI_UNIT($,.STERADIAN.)
SOLID_ANGLE_UNIT()
);
#135288=SHAPE_DEFINITION_REPRESENTATION(#135302,#135337);
#135302=PRODUCT_DEFINITION_SHAPE('',$,#135352);
#135337=SHAPE_REPRESENTATION('',(#32233),#135269);
#135350=PRODUCT_DEFINITION_CONTEXT('part definition',#135394,'design');
#135352=PRODUCT_DEFINITION('2026-10-15-19-09-11-255',
'Dovetail Base Rail',#135366,#135350);
#135366=PRODUCT_DEFINITION_FORMATION('',$,#135397);
#135394=APPLICATION_CONTEXT(
'Core Data for Automotive Mechanical Design Process');
#135395=PRODUCT_CONTEXT('part definition',#135394,'mechanical');
#135397=PRODUCT('2026-10-15-19-09-11-255','Dovetail Base Rail',$,(#135395));
#135411=PRESENTATION_STYLE_ASSIGNMENT((#135425));
#135425=SURFACE_STYLE_USAGE(.BOTH.,#135439);
#135439=SURFACE_SIDE_STYLE('',(#135453));
#135453=SURFACE_STYLE_FILL_AREA(#135467);
#135467=FILL_AREA_STYLE('Opaque(206,210,216)',(#135481));
#135481=FILL_AREA_STYLE_COLOUR('Opaque(206,210,216)',#135495);
#135495=COLOUR_RGB('Opaque(206,210,216)', 0.09019608, 0.27058824, 0.51372549);
ENDSEC;
END-ISO-10303-21;
